ISO-10303-21;
HEADER;
/* Generated by software containing ST-Developer
 * from STEP Tools, Inc. (www.steptools.com) 
 */

FILE_DESCRIPTION(
/* description */ ('Bin tilter linkage'),
/* implementation_level */ '2;1');

FILE_NAME(
/* name */ 'M4 short cap screw (17).step',
/* time_stamp */ '2026-10-28T03:26:24-07:00',
/* author */ (''),
/* organization */ (''),
/* preprocessor_version */ 'ST-DEVELOPER v20.2',
/* originating_system */ 'Autodesk Translation Framework v15.17.0.0',
/* authorisation */ '');

FILE_SCHEMA (('AUTOMOTIVE_DESIGN { 1 0 10303 214 3 1 1 }'));
ENDSEC;

DATA;
#10=MECHANICAL_DESIGN_GEOMETRIC_PRESENTATION_REPRESENTATION('',(#916),#23728);
#704=SHAPE_REPRESENTATION_RELATIONSHIP('SRR','None',#24170,#810);
#810=ADVANCED_BREP_SHAPE_REPRESENTATION('',(#1029),#23670);
#916=STYLED_ITEM('',(#24772),#1029);
#1029=MANIFOLD_SOLID_BREP('Body1',#12447);
#1341=FACE_BOUND('',#3328,.T.);
#1686=PLANE('',#14561);
#1687=PLANE('',#14566);
#1688=PLANE('',#14569);
#2296=FACE_OUTER_BOUND('',#3327,.T.);
#2297=FACE_OUTER_BOUND('',#3329,.T.);
#2298=FACE_OUTER_BOUND('',#3330,.T.);
#2299=FACE_OUTER_BOUND('',#3331,.T.);
#2300=FACE_OUTER_BOUND('',#3332,.T.);
#3327=EDGE_LOOP('',(#9925));
#3328=EDGE_LOOP('',(#9926));
#3329=EDGE_LOOP('',(#9927,#9928,#9929,#9930));
#3330=EDGE_LOOP('',(#9931));
#3331=EDGE_LOOP('',(#9932,#9933,#9934,#9935));
#3332=EDGE_LOOP('',(#9936));
#4205=LINE('',#21509,#4880);
#4206=LINE('',#21515,#4881);
#4880=VECTOR('',#17608,0.350000000000001);
#4881=VECTOR('',#17617,0.199999999999999);
#5619=CIRCLE('',#14562,0.350000000000001);
#5620=CIRCLE('',#14563,0.199999999999999);
#5621=CIRCLE('',#14565,0.350000000000001);
#5622=CIRCLE('',#14568,0.199999999999999);
#6473=VERTEX_POINT('',#21503);
#6474=VERTEX_POINT('',#21505);
#6475=VERTEX_POINT('',#21508);
#6476=VERTEX_POINT('',#21513);
#7702=EDGE_CURVE('',#6473,#6473,#5619,.T.);
#7703=EDGE_CURVE('',#6474,#6474,#5620,.T.);
#7704=EDGE_CURVE('',#6473,#6475,#4205,.T.);
#7705=EDGE_CURVE('',#6475,#6475,#5621,.T.);
#7706=EDGE_CURVE('',#6476,#6476,#5622,.T.);
#7707=EDGE_CURVE('',#6476,#6474,#4206,.T.);
#9925=ORIENTED_EDGE('',*,*,#7702,.T.);
#9926=ORIENTED_EDGE('',*,*,#7703,.F.);
#9927=ORIENTED_EDGE('',*,*,#7702,.F.);
#9928=ORIENTED_EDGE('',*,*,#7704,.T.);
#9929=ORIENTED_EDGE('',*,*,#7705,.T.);
#9930=ORIENTED_EDGE('',*,*,#7704,.F.);
#9931=ORIENTED_EDGE('',*,*,#7705,.F.);
#9932=ORIENTED_EDGE('',*,*,#7706,.F.);
#9933=ORIENTED_EDGE('',*,*,#7707,.T.);
#9934=ORIENTED_EDGE('',*,*,#7703,.T.);
#9935=ORIENTED_EDGE('',*,*,#7707,.F.);
#9936=ORIENTED_EDGE('',*,*,#7706,.T.);
#11475=CYLINDRICAL_SURFACE('',#14564,0.350000000000001);
#11476=CYLINDRICAL_SURFACE('',#14567,0.199999999999999);
#12021=ADVANCED_FACE('',(#2296,#1341),#1686,.T.);
#12022=ADVANCED_FACE('',(#2297),#11475,.T.);
#12023=ADVANCED_FACE('',(#2298),#1687,.F.);
#12024=ADVANCED_FACE('',(#2299),#11476,.T.);
#12025=ADVANCED_FACE('',(#2300),#1688,.T.);
#12447=CLOSED_SHELL('',(#12021,#12022,#12023,#12024,#12025));
#14560=AXIS2_PLACEMENT_3D('',#21501,#17598,#17599);
#14561=AXIS2_PLACEMENT_3D('',#21502,#17600,#17601);
#14562=AXIS2_PLACEMENT_3D('',#21504,#17602,#17603);
#14563=AXIS2_PLACEMENT_3D('',#21506,#17604,#17605);
#14564=AXIS2_PLACEMENT_3D('',#21507,#17606,#17607);
#14565=AXIS2_PLACEMENT_3D('',#21510,#17609,#17610);
#14566=AXIS2_PLACEMENT_3D('',#21511,#17611,#17612);
#14567=AXIS2_PLACEMENT_3D('',#21512,#17613,#17614);
#14568=AXIS2_PLACEMENT_3D('',#21514,#17615,#17616);
#14569=AXIS2_PLACEMENT_3D('',#21516,#17618,#17619);
#17598=DIRECTION('axis',(0.,0.,1.));
#17599=DIRECTION('refdir',(1.,0.,0.));
#17600=DIRECTION('center_axis',(0.,1.,0.));
#17601=DIRECTION('ref_axis',(1.,0.,0.));
#17602=DIRECTION('center_axis',(0.,1.,0.));
#17603=DIRECTION('ref_axis',(1.,0.,0.));
#17604=DIRECTION('center_axis',(0.,1.,0.));
#17605=DIRECTION('ref_axis',(1.,0.,0.));
#17606=DIRECTION('center_axis',(0.,1.,0.));
#17607=DIRECTION('ref_axis',(1.,0.,0.));
#17608=DIRECTION('',(0.,-1.,0.));
#17609=DIRECTION('center_axis',(0.,1.,0.));
#17610=DIRECTION('ref_axis',(1.,0.,0.));
#17611=DIRECTION('center_axis',(0.,1.,0.));
#17612=DIRECTION('ref_axis',(1.,0.,0.));
#17613=DIRECTION('center_axis',(0.,1.,0.));
#17614=DIRECTION('ref_axis',(1.,0.,0.));
#17615=DIRECTION('center_axis',(0.,1.,0.));
#17616=DIRECTION('ref_axis',(1.,0.,0.));
#17617=DIRECTION('',(0.,-1.,0.));
#17618=DIRECTION('center_axis',(0.,1.,0.));
#17619=DIRECTION('ref_axis',(1.,0.,0.));
#21501=CARTESIAN_POINT('',(0.,0.,0.));
#21502=CARTESIAN_POINT('Origin',(16.6918524548049,-0.8,16.3081475451951));
#21503=CARTESIAN_POINT('',(16.3418524548049,-0.8,16.3081475451951));
#21504=CARTESIAN_POINT('Origin',(16.6918524548049,-0.8,16.3081475451951));
#21505=CARTESIAN_POINT('',(16.4918524548049,-0.8,16.3081475451951));
#21506=CARTESIAN_POINT('Origin',(16.6918524548049,-0.8,16.3081475451951));
#21507=CARTESIAN_POINT('Origin',(16.6918524548049,-1.2,16.3081475451951));
#21508=CARTESIAN_POINT('',(16.3418524548049,-1.2,16.3081475451951));
#21509=CARTESIAN_POINT('',(16.3418524548049,-1.2,16.3081475451951));
#21510=CARTESIAN_POINT('Origin',(16.6918524548049,-1.2,16.3081475451951));
#21511=CARTESIAN_POINT('Origin',(16.6918524548049,-1.2,16.3081475451951));
#21512=CARTESIAN_POINT('Origin',(16.6918524548049,-0.8,16.3081475451951));
#21513=CARTESIAN_POINT('',(16.4918524548049,-0.1,16.3081475451951));
#21514=CARTESIAN_POINT('Origin',(16.6918524548049,-0.1,16.3081475451951));
#21515=CARTESIAN_POINT('',(16.4918524548049,-0.8,16.3081475451951));
#21516=CARTESIAN_POINT('Origin',(16.6918524548049,-0.1,16.3081475451951));
#23553=UNCERTAINTY_MEASURE_WITH_UNIT(LENGTH_MEASURE(0.001),#23729,
'DISTANCE_ACCURACY_VALUE',
'Maximum model space distance between geometric entities at asserted c
onnectivities');
#23611=UNCERTAINTY_MEASURE_WITH_UNIT(LENGTH_MEASURE(0.001),#23729,
'DISTANCE_ACCURACY_VALUE',
'Maximum model space distance between geometric entities at asserted c
onnectivities');
#23670=(
GEOMETRIC_REPRESENTATION_CONTEXT(3)
GLOBAL_UNCERTAINTY_ASSIGNED_CONTEXT((#23553))
GLOBAL_UNIT_ASSIGNED_CONTEXT((#23729,#23731,#23732))
REPRESENTATION_CONTEXT('','3D')
);
#23728=(
GEOMETRIC_REPRESENTATION_CONTEXT(3)
GLOBAL_UNCERTAINTY_ASSIGNED_CONTEXT((#23611))
GLOBAL_UNIT_ASSIGNED_CONTEXT((#23729,#23731,#23732))
REPRESENTATION_CONTEXT('','3D')
);
#23729=(
LENGTH_UNIT()
NAMED_UNIT(*)
SI_UNIT(.CENTI.,.METRE.)
);
#23731=(
NAMED_UNIT(*)
PLANE_ANGLE_UNIT()
SI_UNIT($,.RADIAN.)
);
#23732=(
NAMED_UNIT(*)
SI_UNIT($,.STERADIAN.)
SOLID_ANGLE_UNIT()
);
#23791=SHAPE_DEFINITION_REPRESENTATION(#23907,#24170);
#23907=PRODUCT_DEFINITION_SHAPE('',$,#24287);
#24170=SHAPE_REPRESENTATION('',(#14560),#23670);
#24228=PRODUCT_DEFINITION_CONTEXT('part definition',#24578,'design');
#24287=PRODUCT_DEFINITION('M4 short cap screw (17)',
'M4 short cap screw (17)',#24403,#24228);
#24403=PRODUCT_DEFINITION_FORMATION('',$,#24638);
#24578=APPLICATION_CONTEXT(
'Core Data for Automotive Mechanical Design Process');
#24579=PRODUCT_CONTEXT('part definition',#24578,'mechanical');
#24638=PRODUCT('M4 short cap screw (17)','M4 short cap screw (17)',
'M4 short cap screw (17)',(#24579));
#24766=COLOUR_RGB('Black',0.12,0.14,0.17);
#24767=FILL_AREA_STYLE_COLOUR('',#24766);
#24768=FILL_AREA_STYLE('',(#24767));
#24769=SURFACE_STYLE_FILL_AREA(#24768);
#24770=SURFACE_SIDE_STYLE('',(#24769));
#24771=SURFACE_STYLE_USAGE(.BOTH.,#24770);
#24772=PRESENTATION_STYLE_ASSIGNMENT((#24771));
ENDSEC;
END-ISO-10303-21;
